ISO-10303-21;
HEADER;
/* Generated by software containing ST-Developer
 * from STEP Tools, Inc. (www.steptools.com) 
 */

FILE_DESCRIPTION(
/* description */ ('Torque wrench calibration arm'),
/* implementation_level */ '2;1');

FILE_NAME(
/* name */ 'Bonded foot (1).step',
/* time_stamp */ '2026-10-28T03:24:52-07:00',
/* author */ (''),
/* organization */ (''),
/* preprocessor_version */ 'ST-DEVELOPER v20.2',
/* originating_system */ 'Autodesk Translation Framework v15.17.0.0',
/* authorisation */ '');

FILE_SCHEMA (('AUTOMOTIVE_DESIGN { 1 0 10303 214 3 1 1 }'));
ENDSEC;

DATA;
#10=MECHANICAL_DESIGN_GEOMETRIC_PRESENTATION_REPRESENTATION('',(#432),#12783);
#358=SHAPE_REPRESENTATION_RELATIONSHIP('SRR','None',#12939,#395);
#395=ADVANCED_BREP_SHAPE_REPRESENTATION('',(#486),#12748);
#432=STYLED_ITEM('',(#13226),#486);
#486=MANIFOLD_SOLID_BREP('Body1',#6501);
#704=PLANE('',#7151);
#705=PLANE('',#7152);
#706=PLANE('',#7153);
#707=PLANE('',#7154);
#708=PLANE('',#7155);
#709=PLANE('',#7156);
#969=FACE_OUTER_BOUND('',#1416,.T.);
#970=FACE_OUTER_BOUND('',#1417,.T.);
#971=FACE_OUTER_BOUND('',#1418,.T.);
#972=FACE_OUTER_BOUND('',#1419,.T.);
#973=FACE_OUTER_BOUND('',#1420,.T.);
#974=FACE_OUTER_BOUND('',#1421,.T.);
#1416=EDGE_LOOP('',(#4771,#4772,#4773,#4774));
#1417=EDGE_LOOP('',(#4775,#4776,#4777,#4778));
#1418=EDGE_LOOP('',(#4779,#4780,#4781,#4782));
#1419=EDGE_LOOP('',(#4783,#4784,#4785,#4786));
#1420=EDGE_LOOP('',(#4787,#4788,#4789,#4790));
#1421=EDGE_LOOP('',(#4791,#4792,#4793,#4794));
#1908=LINE('',#10381,#2323);
#1909=LINE('',#10383,#2324);
#1910=LINE('',#10385,#2325);
#1911=LINE('',#10386,#2326);
#1912=LINE('',#10389,#2327);
#1913=LINE('',#10391,#2328);
#1914=LINE('',#10392,#2329);
#1915=LINE('',#10395,#2330);
#1916=LINE('',#10397,#2331);
#1917=LINE('',#10398,#2332);
#1918=LINE('',#10400,#2333);
#1919=LINE('',#10401,#2334);
#2323=VECTOR('',#8316,1.);
#2324=VECTOR('',#8317,1.);
#2325=VECTOR('',#8318,1.);
#2326=VECTOR('',#8319,1.);
#2327=VECTOR('',#8322,1.);
#2328=VECTOR('',#8323,1.);
#2329=VECTOR('',#8324,1.);
#2330=VECTOR('',#8327,1.);
#2331=VECTOR('',#8328,1.);
#2332=VECTOR('',#8329,1.);
#2333=VECTOR('',#8332,1.);
#2334=VECTOR('',#8333,1.);
#3111=VERTEX_POINT('',#10379);
#3112=VERTEX_POINT('',#10380);
#3113=VERTEX_POINT('',#10382);
#3114=VERTEX_POINT('',#10384);
#3115=VERTEX_POINT('',#10388);
#3116=VERTEX_POINT('',#10390);
#3117=VERTEX_POINT('',#10394);
#3118=VERTEX_POINT('',#10396);
#3743=EDGE_CURVE('',#3111,#3112,#1908,.T.);
#3744=EDGE_CURVE('',#3112,#3113,#1909,.T.);
#3745=EDGE_CURVE('',#3114,#3113,#1910,.T.);
#3746=EDGE_CURVE('',#3111,#3114,#1911,.T.);
#3747=EDGE_CURVE('',#3115,#3111,#1912,.T.);
#3748=EDGE_CURVE('',#3116,#3114,#1913,.T.);
#3749=EDGE_CURVE('',#3115,#3116,#1914,.T.);
#3750=EDGE_CURVE('',#3117,#3115,#1915,.T.);
#3751=EDGE_CURVE('',#3118,#3116,#1916,.T.);
#3752=EDGE_CURVE('',#3117,#3118,#1917,.T.);
#3753=EDGE_CURVE('',#3112,#3117,#1918,.T.);
#3754=EDGE_CURVE('',#3113,#3118,#1919,.T.);
#4771=ORIENTED_EDGE('',*,*,#3743,.T.);
#4772=ORIENTED_EDGE('',*,*,#3744,.T.);
#4773=ORIENTED_EDGE('',*,*,#3745,.F.);
#4774=ORIENTED_EDGE('',*,*,#3746,.F.);
#4775=ORIENTED_EDGE('',*,*,#3747,.T.);
#4776=ORIENTED_EDGE('',*,*,#3746,.T.);
#4777=ORIENTED_EDGE('',*,*,#3748,.F.);
#4778=ORIENTED_EDGE('',*,*,#3749,.F.);
#4779=ORIENTED_EDGE('',*,*,#3750,.T.);
#4780=ORIENTED_EDGE('',*,*,#3749,.T.);
#4781=ORIENTED_EDGE('',*,*,#3751,.F.);
#4782=ORIENTED_EDGE('',*,*,#3752,.F.);
#4783=ORIENTED_EDGE('',*,*,#3753,.T.);
#4784=ORIENTED_EDGE('',*,*,#3752,.T.);
#4785=ORIENTED_EDGE('',*,*,#3754,.F.);
#4786=ORIENTED_EDGE('',*,*,#3744,.F.);
#4787=ORIENTED_EDGE('',*,*,#3754,.T.);
#4788=ORIENTED_EDGE('',*,*,#3751,.T.);
#4789=ORIENTED_EDGE('',*,*,#3748,.T.);
#4790=ORIENTED_EDGE('',*,*,#3745,.T.);
#4791=ORIENTED_EDGE('',*,*,#3753,.F.);
#4792=ORIENTED_EDGE('',*,*,#3743,.F.);
#4793=ORIENTED_EDGE('',*,*,#3747,.F.);
#4794=ORIENTED_EDGE('',*,*,#3750,.F.);
#6194=ADVANCED_FACE('',(#969),#704,.T.);
#6195=ADVANCED_FACE('',(#970),#705,.T.);
#6196=ADVANCED_FACE('',(#971),#706,.T.);
#6197=ADVANCED_FACE('',(#972),#707,.T.);
#6198=ADVANCED_FACE('',(#973),#708,.T.);
#6199=ADVANCED_FACE('',(#974),#709,.F.);
#6501=CLOSED_SHELL('',(#6194,#6195,#6196,#6197,#6198,#6199));
#7150=AXIS2_PLACEMENT_3D('',#10377,#8312,#8313);
#7151=AXIS2_PLACEMENT_3D('',#10378,#8314,#8315);
#7152=AXIS2_PLACEMENT_3D('',#10387,#8320,#8321);
#7153=AXIS2_PLACEMENT_3D('',#10393,#8325,#8326);
#7154=AXIS2_PLACEMENT_3D('',#10399,#8330,#8331);
#7155=AXIS2_PLACEMENT_3D('',#10402,#8334,#8335);
#7156=AXIS2_PLACEMENT_3D('',#10403,#8336,#8337);
#8312=DIRECTION('axis',(0.,0.,1.));
#8313=DIRECTION('refdir',(1.,0.,0.));
#8314=DIRECTION('center_axis',(0.,1.,0.));
#8315=DIRECTION('ref_axis',(-1.,0.,0.));
#8316=DIRECTION('',(-1.,0.,0.));
#8317=DIRECTION('',(0.,0.,1.));
#8318=DIRECTION('',(-1.,0.,0.));
#8319=DIRECTION('',(0.,0.,1.));
#8320=DIRECTION('center_axis',(1.,0.,0.));
#8321=DIRECTION('ref_axis',(0.,1.,0.));
#8322=DIRECTION('',(0.,1.,0.));
#8323=DIRECTION('',(0.,1.,0.));
#8324=DIRECTION('',(0.,0.,1.));
#8325=DIRECTION('center_axis',(0.,-1.,0.));
#8326=DIRECTION('ref_axis',(1.,0.,0.));
#8327=DIRECTION('',(1.,0.,0.));
#8328=DIRECTION('',(1.,0.,0.));
#8329=DIRECTION('',(0.,0.,1.));
#8330=DIRECTION('center_axis',(-1.,0.,0.));
#8331=DIRECTION('ref_axis',(0.,-1.,0.));
#8332=DIRECTION('',(0.,-1.,0.));
#8333=DIRECTION('',(0.,-1.,0.));
#8334=DIRECTION('center_axis',(0.,0.,1.));
#8335=DIRECTION('ref_axis',(1.,0.,0.));
#8336=DIRECTION('center_axis',(0.,0.,1.));
#8337=DIRECTION('ref_axis',(1.,0.,0.));
#10377=CARTESIAN_POINT('',(0.,0.,0.));
#10378=CARTESIAN_POINT('Origin',(11.,10.5,-0.8));
#10379=CARTESIAN_POINT('',(11.,10.5,-0.8));
#10380=CARTESIAN_POINT('',(9.,10.5,-0.8));
#10381=CARTESIAN_POINT('',(11.,10.5,-0.8));
#10382=CARTESIAN_POINT('',(9.,10.5,0.));
#10383=CARTESIAN_POINT('',(9.,10.5,-0.8));
#10384=CARTESIAN_POINT('',(11.,10.5,0.));
#10385=CARTESIAN_POINT('',(11.,10.5,0.));
#10386=CARTESIAN_POINT('',(11.,10.5,-0.8));
#10387=CARTESIAN_POINT('Origin',(11.,-2.,-0.8));
#10388=CARTESIAN_POINT('',(11.,-2.,-0.8));
#10389=CARTESIAN_POINT('',(11.,-2.,-0.8));
#10390=CARTESIAN_POINT('',(11.,-2.,0.));
#10391=CARTESIAN_POINT('',(11.,-2.,0.));
#10392=CARTESIAN_POINT('',(11.,-2.,-0.8));
#10393=CARTESIAN_POINT('Origin',(9.,-2.,-0.8));
#10394=CARTESIAN_POINT('',(9.,-2.,-0.8));
#10395=CARTESIAN_POINT('',(9.,-2.,-0.8));
#10396=CARTESIAN_POINT('',(9.,-2.,0.));
#10397=CARTESIAN_POINT('',(9.,-2.,0.));
#10398=CARTESIAN_POINT('',(9.,-2.,-0.8));
#10399=CARTESIAN_POINT('Origin',(9.,10.5,-0.8));
#10400=CARTESIAN_POINT('',(9.,10.5,-0.8));
#10401=CARTESIAN_POINT('',(9.,10.5,0.));
#10402=CARTESIAN_POINT('Origin',(10.,4.25,0.));
#10403=CARTESIAN_POINT('Origin',(10.,4.25,-0.8));
#12704=UNCERTAINTY_MEASURE_WITH_UNIT(LENGTH_MEASURE(0.001),#12784,
'DISTANCE_ACCURACY_VALUE',
'Maximum model space distance between geometric entities at asserted c
onnectivities');
#12739=UNCERTAINTY_MEASURE_WITH_UNIT(LENGTH_MEASURE(0.001),#12784,
'DISTANCE_ACCURACY_VALUE',
'Maximum model space distance between geometric entities at asserted c
onnectivities');
#12748=(
GEOMETRIC_REPRESENTATION_CONTEXT(3)
GLOBAL_UNCERTAINTY_ASSIGNED_CONTEXT((#12704))
GLOBAL_UNIT_ASSIGNED_CONTEXT((#12784,#12786,#12787))
REPRESENTATION_CONTEXT('','3D')
);
#12783=(
GEOMETRIC_REPRESENTATION_CONTEXT(3)
GLOBAL_UNCERTAINTY_ASSIGNED_CONTEXT((#12739))
GLOBAL_UNIT_ASSIGNED_CONTEXT((#12784,#12786,#12787))
REPRESENTATION_CONTEXT('','3D')
);
#12784=(
LENGTH_UNIT()
NAMED_UNIT(*)
SI_UNIT(.CENTI.,.METRE.)
);
#12786=(
NAMED_UNIT(*)
PLANE_ANGLE_UNIT()
SI_UNIT($,.RADIAN.)
);
#12787=(
NAMED_UNIT(*)
SI_UNIT($,.STERADIAN.)
SOLID_ANGLE_UNIT()
);
#12796=SHAPE_DEFINITION_REPRESENTATION(#12839,#12939);
#12839=PRODUCT_DEFINITION_SHAPE('',$,#12983);
#12939=SHAPE_REPRESENTATION('',(#7150),#12748);
#12974=PRODUCT_DEFINITION_CONTEXT('part definition',#13105,'design');
#12983=PRODUCT_DEFINITION('Bonded foot (1)','Bonded foot (1)',#13026,#12974);
#13026=PRODUCT_DEFINITION_FORMATION('',$,#13115);
#13105=APPLICATION_CONTEXT(
'Core Data for Automotive Mechanical Design Process');
#13106=PRODUCT_CONTEXT('part definition',#13105,'mechanical');
#13115=PRODUCT('Bonded foot (1)','Bonded foot (1)','Bonded foot (1)',(#13106));
#13220=COLOUR_RGB('Off White',0.89,0.88,0.83);
#13221=FILL_AREA_STYLE_COLOUR('',#13220);
#13222=FILL_AREA_STYLE('',(#13221));
#13223=SURFACE_STYLE_FILL_AREA(#13222);
#13224=SURFACE_SIDE_STYLE('',(#13223));
#13225=SURFACE_STYLE_USAGE(.BOTH.,#13224);
#13226=PRESENTATION_STYLE_ASSIGNMENT((#13225));
ENDSEC;
END-ISO-10303-21;
